ISO-10303-21;
HEADER;
/* Generated by software containing ST-Developer
 * from STEP Tools, Inc. (www.steptools.com) 
 */

FILE_DESCRIPTION(
/* description */ ('STEP AP214'),
/* implementation_level */ '2;1');

FILE_NAME(
/* name */ 'PRT-TQ-1020.step',
/* time_stamp */ '2026-10-07T12:49:37-07:00',
/* author */ (''),
/* organization */ (''),
/* preprocessor_version */ 'ST-DEVELOPER v20.2',
/* originating_system */ 'Autodesk Translation Framework v15.15.0.0',
/* authorisation */ '');

FILE_SCHEMA (('AUTOMOTIVE_DESIGN { 1 0 10303 214 3 1 1 }'));
ENDSEC;

DATA;
#10=MECHANICAL_DESIGN_GEOMETRIC_PRESENTATION_REPRESENTATION('',(#308),#33016);
#250=SHAPE_REPRESENTATION_RELATIONSHIP('SRR','None',#33144,#277);
#277=ADVANCED_BREP_SHAPE_REPRESENTATION('',(#335),#33005);
#308=STYLED_ITEM('',(#33288),#335);
#335=MANIFOLD_SOLID_BREP('Body1',#9959);
#522=FACE_BOUND('',#2001,.T.);
#523=FACE_BOUND('',#2003,.T.);
#962=PLANE('',#10882);
#963=PLANE('',#10885);
#1396=FACE_OUTER_BOUND('',#2000,.T.);
#1397=FACE_OUTER_BOUND('',#2002,.T.);
#1398=FACE_OUTER_BOUND('',#2004,.T.);
#1399=FACE_OUTER_BOUND('',#2005,.T.);
#2000=EDGE_LOOP('',(#8306));
#2001=EDGE_LOOP('',(#8307));
#2002=EDGE_LOOP('',(#8308));
#2003=EDGE_LOOP('',(#8309));
#2004=EDGE_LOOP('',(#8310,#8311,#8312,#8313));
#2005=EDGE_LOOP('',(#8314,#8315,#8316,#8317));
#2464=CIRCLE('',#10883,9.15);
#2465=CIRCLE('',#10884,7.25);
#2466=CIRCLE('',#10886,9.15);
#2467=CIRCLE('',#10887,7.25);
#3178=LINE('',#27981,#3928);
#3179=LINE('',#27983,#3929);
#3928=VECTOR('',#13055,9.15);
#3929=VECTOR('',#13058,7.25);
#4719=VERTEX_POINT('',#27971);
#4720=VERTEX_POINT('',#27973);
#4721=VERTEX_POINT('',#27976);
#4722=VERTEX_POINT('',#27978);
#5966=EDGE_CURVE('',#4719,#4719,#2464,.T.);
#5967=EDGE_CURVE('',#4720,#4720,#2465,.T.);
#5968=EDGE_CURVE('',#4721,#4721,#2466,.T.);
#5969=EDGE_CURVE('',#4722,#4722,#2467,.T.);
#5970=EDGE_CURVE('',#4721,#4719,#3178,.T.);
#5971=EDGE_CURVE('',#4720,#4722,#3179,.T.);
#8306=ORIENTED_EDGE('',*,*,#5966,.T.);
#8307=ORIENTED_EDGE('',*,*,#5967,.F.);
#8308=ORIENTED_EDGE('',*,*,#5968,.F.);
#8309=ORIENTED_EDGE('',*,*,#5969,.T.);
#8310=ORIENTED_EDGE('',*,*,#5968,.T.);
#8311=ORIENTED_EDGE('',*,*,#5970,.T.);
#8312=ORIENTED_EDGE('',*,*,#5966,.F.);
#8313=ORIENTED_EDGE('',*,*,#5970,.F.);
#8314=ORIENTED_EDGE('',*,*,#5967,.T.);
#8315=ORIENTED_EDGE('',*,*,#5971,.T.);
#8316=ORIENTED_EDGE('',*,*,#5969,.F.);
#8317=ORIENTED_EDGE('',*,*,#5971,.F.);
#9316=CYLINDRICAL_SURFACE('',#10888,9.15);
#9317=CYLINDRICAL_SURFACE('',#10889,7.25);
#9762=ADVANCED_FACE('',(#1396,#522),#962,.T.);
#9763=ADVANCED_FACE('',(#1397,#523),#963,.F.);
#9764=ADVANCED_FACE('',(#1398),#9316,.T.);
#9765=ADVANCED_FACE('',(#1399),#9317,.F.);
#9959=CLOSED_SHELL('',(#9762,#9763,#9764,#9765));
#10881=AXIS2_PLACEMENT_3D('',#27969,#13039,#13040);
#10882=AXIS2_PLACEMENT_3D('',#27970,#13041,#13042);
#10883=AXIS2_PLACEMENT_3D('',#27972,#13043,#13044);
#10884=AXIS2_PLACEMENT_3D('',#27974,#13045,#13046);
#10885=AXIS2_PLACEMENT_3D('',#27975,#13047,#13048);
#10886=AXIS2_PLACEMENT_3D('',#27977,#13049,#13050);
#10887=AXIS2_PLACEMENT_3D('',#27979,#13051,#13052);
#10888=AXIS2_PLACEMENT_3D('',#27980,#13053,#13054);
#10889=AXIS2_PLACEMENT_3D('',#27982,#13056,#13057);
#13039=DIRECTION('axis',(0.,0.,1.));
#13040=DIRECTION('refdir',(1.,0.,0.));
#13041=DIRECTION('center_axis',(0.,1.,0.));
#13042=DIRECTION('ref_axis',(0.,0.,1.));
#13043=DIRECTION('center_axis',(0.,1.,0.));
#13044=DIRECTION('ref_axis',(0.,0.,1.));
#13045=DIRECTION('center_axis',(0.,1.,0.));
#13046=DIRECTION('ref_axis',(0.,0.,1.));
#13047=DIRECTION('center_axis',(0.,1.,0.));
#13048=DIRECTION('ref_axis',(0.,0.,1.));
#13049=DIRECTION('center_axis',(0.,1.,0.));
#13050=DIRECTION('ref_axis',(0.,0.,1.));
#13051=DIRECTION('center_axis',(0.,1.,0.));
#13052=DIRECTION('ref_axis',(0.,0.,1.));
#13053=DIRECTION('center_axis',(0.,-1.,0.));
#13054=DIRECTION('ref_axis',(0.,0.,-1.));
#13055=DIRECTION('',(0.,1.,0.));
#13056=DIRECTION('center_axis',(0.,-1.,0.));
#13057=DIRECTION('ref_axis',(0.,0.,-1.));
#13058=DIRECTION('',(0.,-1.,0.));
#27969=CARTESIAN_POINT('',(0.,0.,0.));
#27970=CARTESIAN_POINT('Origin',(0.,13.,0.));
#27971=CARTESIAN_POINT('',(0.,13.,9.15));
#27972=CARTESIAN_POINT('Origin',(0.,13.,0.));
#27973=CARTESIAN_POINT('',(0.,13.,7.25));
#27974=CARTESIAN_POINT('Origin',(0.,13.,0.));
#27975=CARTESIAN_POINT('Origin',(0.,0.,0.));
#27976=CARTESIAN_POINT('',(0.,0.,9.15));
#27977=CARTESIAN_POINT('Origin',(0.,0.,0.));
#27978=CARTESIAN_POINT('',(0.,0.,7.25));
#27979=CARTESIAN_POINT('Origin',(0.,0.,0.));
#27980=CARTESIAN_POINT('Origin',(0.,13.,0.));
#27981=CARTESIAN_POINT('',(-1.12055182121983E-15,13.,9.15));
#27982=CARTESIAN_POINT('Origin',(0.,13.,0.));
#27983=CARTESIAN_POINT('',(-8.87868929381831E-16,13.,7.25));
#32973=UNCERTAINTY_MEASURE_WITH_UNIT(LENGTH_MEASURE(0.01),#33017,
'DISTANCE_ACCURACY_VALUE',
'Maximum model space distance between geometric entities at asserted c
onnectivities');
#32984=UNCERTAINTY_MEASURE_WITH_UNIT(LENGTH_MEASURE(0.01),#33017,
'DISTANCE_ACCURACY_VALUE',
'Maximum model space distance between geometric entities at asserted c
onnectivities');
#33005=(
GEOMETRIC_REPRESENTATION_CONTEXT(3)
GLOBAL_UNCERTAINTY_ASSIGNED_CONTEXT((#32973))
GLOBAL_UNIT_ASSIGNED_CONTEXT((#33017,#33019,#33020))
REPRESENTATION_CONTEXT('','3D')
);
#33016=(
GEOMETRIC_REPRESENTATION_CONTEXT(3)
GLOBAL_UNCERTAINTY_ASSIGNED_CONTEXT((#32984))
GLOBAL_UNIT_ASSIGNED_CONTEXT((#33017,#33019,#33020))
REPRESENTATION_CONTEXT('','3D')
);
#33017=(
LENGTH_UNIT()
NAMED_UNIT(*)
SI_UNIT(.MILLI.,.METRE.)
);
#33019=(
NAMED_UNIT(*)
PLANE_ANGLE_UNIT()
SI_UNIT($,.RADIAN.)
);
#33020=(
NAMED_UNIT(*)
SI_UNIT($,.STERADIAN.)
SOLID_ANGLE_UNIT()
);
#33041=SHAPE_DEFINITION_REPRESENTATION(#33080,#33144);
#33080=PRODUCT_DEFINITION_SHAPE('',$,#33176);
#33144=SHAPE_REPRESENTATION('',(#10881),#33005);
#33155=PRODUCT_DEFINITION_CONTEXT('part definition',#33250,'design');
#33176=PRODUCT_DEFINITION('P_Torque Wrench_Push Bush_PRT-TQ-1020',
'PRT-TQ-1020',#33207,#33155);
#33207=PRODUCT_DEFINITION_FORMATION('',$,#33272);
#33250=APPLICATION_CONTEXT(
'Core Data for Automotive Mechanical Design Process');
#33251=PRODUCT_CONTEXT('part definition',#33250,'mechanical');
#33272=PRODUCT('P_Torque Wrench_Push Bush_PRT-TQ-1020','PRT-TQ-1020',$,
(#33251));
#33288=PRESENTATION_STYLE_ASSIGNMENT((#33295));
#33295=SURFACE_STYLE_USAGE(.BOTH.,#33302);
#33302=SURFACE_SIDE_STYLE('',(#33309));
#33309=SURFACE_STYLE_FILL_AREA(#33316);
#33316=FILL_AREA_STYLE('Opaque(192,192,192)',(#33323));
#33323=FILL_AREA_STYLE_COLOUR('Opaque(192,192,192)',#33330);
#33330=COLOUR_RGB('Opaque(192,192,192)', 0.72549020, 0.75294118, 0.79215686);
ENDSEC;
END-ISO-10303-21;
